ISO-10303-21;
HEADER;
/* Generated by software containing ST-Developer
 * from STEP Tools, Inc. (www.steptools.com) 
 */

FILE_DESCRIPTION(
/* description */ ('Flange-mounted spindle'),
/* implementation_level */ '2;1');

FILE_NAME(
/* name */ 'Flat Washer - M8.step',
/* time_stamp */ '2026-10-27T10:49:51-07:00',
/* author */ (''),
/* organization */ (''),
/* preprocessor_version */ 'ST-DEVELOPER v20.2',
/* originating_system */ 'Autodesk Translation Framework v15.17.0.0',
/* authorisation */ '');

FILE_SCHEMA (('AUTOMOTIVE_DESIGN { 1 0 10303 214 3 1 1 }'));
ENDSEC;

DATA;
#10=MECHANICAL_DESIGN_GEOMETRIC_PRESENTATION_REPRESENTATION('',(#364),#11764);
#309=SHAPE_REPRESENTATION_RELATIONSHIP('SRR','None',#11907,#336);
#336=ADVANCED_BREP_SHAPE_REPRESENTATION('',(#389),#11762);
#364=STYLED_ITEM('',(#12106),#389);
#389=MANIFOLD_SOLID_BREP('Body1',#6159);
#502=FACE_BOUND('',#1463,.T.);
#503=FACE_BOUND('',#1465,.T.);
#664=PLANE('',#7145);
#665=PLANE('',#7146);
#1004=FACE_OUTER_BOUND('',#1460,.T.);
#1005=FACE_OUTER_BOUND('',#1461,.T.);
#1006=FACE_OUTER_BOUND('',#1462,.T.);
#1007=FACE_OUTER_BOUND('',#1464,.T.);
#1460=EDGE_LOOP('',(#5563,#5564,#5565,#5566));
#1461=EDGE_LOOP('',(#5567,#5568,#5569,#5570));
#1462=EDGE_LOOP('',(#5571));
#1463=EDGE_LOOP('',(#5572));
#1464=EDGE_LOOP('',(#5573));
#1465=EDGE_LOOP('',(#5574));
#1890=LINE('',#11569,#2312);
#1891=LINE('',#11575,#2313);
#2312=VECTOR('',#8983,0.42);
#2313=VECTOR('',#8990,0.8);
#2641=CIRCLE('',#7140,0.42);
#2642=CIRCLE('',#7141,0.42);
#2643=CIRCLE('',#7143,0.8);
#2644=CIRCLE('',#7144,0.8);
#3175=VERTEX_POINT('',#11566);
#3176=VERTEX_POINT('',#11568);
#3177=VERTEX_POINT('',#11572);
#3178=VERTEX_POINT('',#11574);
#3974=EDGE_CURVE('',#3175,#3175,#2641,.T.);
#3975=EDGE_CURVE('',#3175,#3176,#1890,.T.);
#3976=EDGE_CURVE('',#3176,#3176,#2642,.T.);
#3977=EDGE_CURVE('',#3177,#3177,#2643,.T.);
#3978=EDGE_CURVE('',#3177,#3178,#1891,.T.);
#3979=EDGE_CURVE('',#3178,#3178,#2644,.T.);
#5563=ORIENTED_EDGE('',*,*,#3974,.F.);
#5564=ORIENTED_EDGE('',*,*,#3975,.T.);
#5565=ORIENTED_EDGE('',*,*,#3976,.T.);
#5566=ORIENTED_EDGE('',*,*,#3975,.F.);
#5567=ORIENTED_EDGE('',*,*,#3977,.F.);
#5568=ORIENTED_EDGE('',*,*,#3978,.T.);
#5569=ORIENTED_EDGE('',*,*,#3979,.T.);
#5570=ORIENTED_EDGE('',*,*,#3978,.F.);
#5571=ORIENTED_EDGE('',*,*,#3977,.T.);
#5572=ORIENTED_EDGE('',*,*,#3974,.T.);
#5573=ORIENTED_EDGE('',*,*,#3979,.F.);
#5574=ORIENTED_EDGE('',*,*,#3976,.F.);
#5782=CYLINDRICAL_SURFACE('',#7139,0.42);
#5783=CYLINDRICAL_SURFACE('',#7142,0.8);
#6115=ADVANCED_FACE('',(#1004),#5782,.F.);
#6116=ADVANCED_FACE('',(#1005),#5783,.T.);
#6117=ADVANCED_FACE('',(#1006,#502),#664,.T.);
#6118=ADVANCED_FACE('',(#1007,#503),#665,.F.);
#6159=CLOSED_SHELL('',(#6115,#6116,#6117,#6118));
#7138=AXIS2_PLACEMENT_3D('',#11564,#8977,#8978);
#7139=AXIS2_PLACEMENT_3D('',#11565,#8979,#8980);
#7140=AXIS2_PLACEMENT_3D('',#11567,#8981,#8982);
#7141=AXIS2_PLACEMENT_3D('',#11570,#8984,#8985);
#7142=AXIS2_PLACEMENT_3D('',#11571,#8986,#8987);
#7143=AXIS2_PLACEMENT_3D('',#11573,#8988,#8989);
#7144=AXIS2_PLACEMENT_3D('',#11576,#8991,#8992);
#7145=AXIS2_PLACEMENT_3D('',#11577,#8993,#8994);
#7146=AXIS2_PLACEMENT_3D('',#11578,#8995,#8996);
#8977=DIRECTION('axis',(0.,0.,1.));
#8978=DIRECTION('refdir',(1.,0.,0.));
#8979=DIRECTION('center_axis',(0.,1.,0.));
#8980=DIRECTION('ref_axis',(1.,0.,0.));
#8981=DIRECTION('center_axis',(0.,-1.,0.));
#8982=DIRECTION('ref_axis',(1.,0.,0.));
#8983=DIRECTION('',(0.,-1.,0.));
#8984=DIRECTION('center_axis',(0.,-1.,0.));
#8985=DIRECTION('ref_axis',(1.,0.,0.));
#8986=DIRECTION('center_axis',(0.,1.,0.));
#8987=DIRECTION('ref_axis',(1.,0.,0.));
#8988=DIRECTION('center_axis',(0.,1.,0.));
#8989=DIRECTION('ref_axis',(1.,0.,0.));
#8990=DIRECTION('',(0.,-1.,0.));
#8991=DIRECTION('center_axis',(0.,1.,0.));
#8992=DIRECTION('ref_axis',(1.,0.,0.));
#8993=DIRECTION('center_axis',(0.,1.,0.));
#8994=DIRECTION('ref_axis',(1.,0.,0.));
#8995=DIRECTION('center_axis',(0.,1.,0.));
#8996=DIRECTION('ref_axis',(1.,0.,0.));
#11564=CARTESIAN_POINT('',(0.,0.,0.));
#11565=CARTESIAN_POINT('Origin',(0.,0.,0.));
#11566=CARTESIAN_POINT('',(-0.42,0.16,5.14351655641888E-17));
#11567=CARTESIAN_POINT('Origin',(0.,0.16,0.));
#11568=CARTESIAN_POINT('',(-0.42,0.,5.14351655641888E-17));
#11569=CARTESIAN_POINT('',(-0.42,0.,5.14351655641888E-17));
#11570=CARTESIAN_POINT('Origin',(0.,0.,0.));
#11571=CARTESIAN_POINT('Origin',(0.,0.,0.));
#11572=CARTESIAN_POINT('',(-0.8,0.16,9.79717439317883E-17));
#11573=CARTESIAN_POINT('Origin',(0.,0.16,0.));
#11574=CARTESIAN_POINT('',(-0.8,0.,9.79717439317883E-17));
#11575=CARTESIAN_POINT('',(-0.8,0.,9.79717439317883E-17));
#11576=CARTESIAN_POINT('Origin',(0.,0.,0.));
#11577=CARTESIAN_POINT('Origin',(0.,0.16,0.));
#11578=CARTESIAN_POINT('Origin',(0.,0.,0.));
#11730=UNCERTAINTY_MEASURE_WITH_UNIT(LENGTH_MEASURE(0.001),#11765,
'DISTANCE_ACCURACY_VALUE',
'Maximum model space distance between geometric entities at asserted c
onnectivities');
#11732=UNCERTAINTY_MEASURE_WITH_UNIT(LENGTH_MEASURE(0.001),#11765,
'DISTANCE_ACCURACY_VALUE',
'Maximum model space distance between geometric entities at asserted c
onnectivities');
#11762=(
GEOMETRIC_REPRESENTATION_CONTEXT(3)
GLOBAL_UNCERTAINTY_ASSIGNED_CONTEXT((#11730))
GLOBAL_UNIT_ASSIGNED_CONTEXT((#11765,#11767,#11768))
REPRESENTATION_CONTEXT('','3D')
);
#11764=(
GEOMETRIC_REPRESENTATION_CONTEXT(3)
GLOBAL_UNCERTAINTY_ASSIGNED_CONTEXT((#11732))
GLOBAL_UNIT_ASSIGNED_CONTEXT((#11765,#11767,#11768))
REPRESENTATION_CONTEXT('','3D')
);
#11765=(
LENGTH_UNIT()
NAMED_UNIT(*)
SI_UNIT(.CENTI.,.METRE.)
);
#11767=(
NAMED_UNIT(*)
PLANE_ANGLE_UNIT()
SI_UNIT($,.RADIAN.)
);
#11768=(
NAMED_UNIT(*)
SI_UNIT($,.STERADIAN.)
SOLID_ANGLE_UNIT()
);
#11798=SHAPE_DEFINITION_REPRESENTATION(#11831,#11907);
#11831=PRODUCT_DEFINITION_SHAPE('',$,#11939);
#11907=SHAPE_REPRESENTATION('',(#7138),#11762);
#11909=PRODUCT_DEFINITION_CONTEXT('part definition',#12004,'design');
#11939=PRODUCT_DEFINITION('Flat Washer - M8','Flat Washer - M8',#11970,
#11909);
#11970=PRODUCT_DEFINITION_FORMATION('',$,#12035);
#12004=APPLICATION_CONTEXT(
'Core Data for Automotive Mechanical Design Process');
#12005=PRODUCT_CONTEXT('part definition',#12004,'mechanical');
#12035=PRODUCT('Flat Washer - M8','Flat Washer - M8','Flat Washer - M8',
(#12005));
#12100=COLOUR_RGB('Black',0.12,0.14,0.17);
#12101=FILL_AREA_STYLE_COLOUR('',#12100);
#12102=FILL_AREA_STYLE('',(#12101));
#12103=SURFACE_STYLE_FILL_AREA(#12102);
#12104=SURFACE_SIDE_STYLE('',(#12103));
#12105=SURFACE_STYLE_USAGE(.BOTH.,#12104);
#12106=PRESENTATION_STYLE_ASSIGNMENT((#12105));
ENDSEC;
END-ISO-10303-21;
